ISO-10303-21;
HEADER;
/* Generated by software containing ST-Developer
 * from STEP Tools, Inc. (www.steptools.com) 
 */

FILE_DESCRIPTION(
/* description */ ('PAT-083'),
/* implementation_level */ '2;1');

FILE_NAME(
/* name */ 'Lower body.step',
/* time_stamp */ '2026-10-29T20:18:00-07:00',
/* author */ (''),
/* organization */ (''),
/* preprocessor_version */ 'ST-DEVELOPER v20.2',
/* originating_system */ 'Autodesk Translation Framework v15.17.0.0',
/* authorisation */ '');

FILE_SCHEMA (('AUTOMOTIVE_DESIGN { 1 0 10303 214 3 1 1 }'));
ENDSEC;

DATA;
#10=MECHANICAL_DESIGN_GEOMETRIC_PRESENTATION_REPRESENTATION('',(#232),#8428);
#167=B_SPLINE_CURVE_WITH_KNOTS('',3,(#5773,#5774,#5775,#5776,#5777,#5778,
#5779,#5780,#5781,#5782,#5783,#5784,#5785,#5786,#5787,#5788,#5789,#5790),
 .UNSPECIFIED.,.F.,.F.,(4,2,2,2,2,2,2,2,4),(0.603815071984235,0.754767131302978,
0.90571919062172,1.0566746672951,1.20763014396847,1.35858562064185,1.50954109731522,
1.66049315663396,1.81144521595271),.UNSPECIFIED.);
#168=B_SPLINE_CURVE_WITH_KNOTS('',3,(#5793,#5794,#5795,#5796,#5797,#5798,
#5799,#5800,#5801,#5802,#5803,#5804,#5805,#5806,#5807,#5808,#5809,#5810,
#5811),.UNSPECIFIED.,.F.,.F.,(4,2,2,2,3,2,2,2,4),(1.81144521595271,1.96239727527145,
2.11334933459019,2.26430481126357,2.41526028793694,2.56621576461032,2.71717124128369,
2.86812330060244,3.01907535992118),.UNSPECIFIED.);
#169=B_SPLINE_CURVE_WITH_KNOTS('',3,(#5826,#5827,#5828,#5829,#5830,#5831,
#5832,#5833,#5834,#5835,#5836,#5837,#5838,#5839,#5840,#5841,#5842,#5843,
#5844,#5845,#5846,#5847,#5848,#5849,#5850,#5851),.UNSPECIFIED.,.F.,.F.,
(4,2,2,2,2,2,2,2,2,2,2,2,4),(0.,0.258582759599652,0.517165519199304,0.775740569348226,
1.03431561949715,1.29289066964607,1.55146571979499,1.81004847939464,2.0686312389943,
2.32721399859395,2.5857967581936,2.84437180834252,3.10294685849144),
 .UNSPECIFIED.);
#170=B_SPLINE_CURVE_WITH_KNOTS('',3,(#5852,#5853,#5854,#5855,#5856,#5857,
#5858,#5859,#5860,#5861),.UNSPECIFIED.,.F.,.F.,(4,2,2,2,4),(3.10294685849144,
3.36152190864037,3.62009695878929,3.87867971838894,4.13726247798859),
 .UNSPECIFIED.);
#171=B_SPLINE_CURVE_WITH_KNOTS('',3,(#5868,#5869,#5870,#5871,#5872,#5873,
#5874,#5875,#5876,#5877,#5878,#5879,#5880,#5881,#5882,#5883,#5884,#5885),
 .UNSPECIFIED.,.F.,.F.,(4,2,2,2,2,2,2,2,4),(0.615024883366032,0.768571244696458,
0.922117606026885,1.07608368637947,1.23004976673206,1.38401584708465,1.53798192743724,
1.69152828876767,1.8450746500981),.UNSPECIFIED.);
#172=B_SPLINE_CURVE_WITH_KNOTS('',3,(#5889,#5890,#5891,#5892,#5893,#5894,
#5895,#5896,#5897,#5898,#5899,#5900,#5901,#5902,#5903,#5904,#5905,#5906,
#5907),.UNSPECIFIED.,.F.,.F.,(4,2,2,2,3,2,2,2,4),(1.8450746500981,1.99862101142852,
2.15216737275895,2.30613345311154,2.46009953346413,2.61406561381672,2.76803169416931,
2.92157805549973,3.07512441683016),.UNSPECIFIED.);
#173=B_SPLINE_CURVE_WITH_KNOTS('',3,(#5916,#5917,#5918,#5919,#5920,#5921,
#5922,#5923,#5924,#5925),.UNSPECIFIED.,.F.,.F.,(4,2,2,2,4),(0.,0.258582759599652,
0.517165519199304,0.775740569348226,1.03431561949715),.UNSPECIFIED.);
#174=B_SPLINE_CURVE_WITH_KNOTS('',3,(#5927,#5928,#5929,#5930,#5931,#5932,
#5933,#5934,#5935,#5936),.UNSPECIFIED.,.F.,.F.,(4,2,2,2,4),(3.10294685849144,
3.36152190864037,3.62009695878929,3.87867971838894,4.13726247798859),
 .UNSPECIFIED.);
#175=B_SPLINE_CURVE_WITH_KNOTS('',3,(#5937,#5938,#5939,#5940,#5941,#5942,
#5943,#5944,#5945,#5946,#5947,#5948,#5949,#5950,#5951,#5952,#5953,#5954),
 .UNSPECIFIED.,.F.,.F.,(4,2,2,2,2,2,2,2,4),(1.03431561949715,1.29289066964607,
1.55146571979499,1.81004847939464,2.0686312389943,2.32721399859395,2.5857967581936,
2.84437180834252,3.10294685849144),.UNSPECIFIED.);
#184=SHAPE_REPRESENTATION_RELATIONSHIP('SRR','None',#8518,#208);
#208=ADVANCED_BREP_SHAPE_REPRESENTATION('',(#256),#8407);
#232=STYLED_ITEM('',(#8684),#256);
#256=MANIFOLD_SOLID_BREP('Body1',#3678);
#283=FACE_BOUND('',#779,.T.);
#284=FACE_BOUND('',#788,.T.);
#285=FACE_BOUND('',#791,.T.);
#286=FACE_BOUND('',#793,.T.);
#287=FACE_BOUND('',#795,.T.);
#288=FACE_BOUND('',#796,.T.);
#289=FACE_BOUND('',#797,.T.);
#290=FACE_BOUND('',#798,.T.);
#291=FACE_BOUND('',#799,.T.);
#292=FACE_BOUND('',#800,.T.);
#293=FACE_BOUND('',#801,.T.);
#294=FACE_BOUND('',#803,.T.);
#295=FACE_BOUND('',#804,.T.);
#296=FACE_BOUND('',#805,.T.);
#374=PLANE('',#4004);
#375=PLANE('',#4008);
#376=PLANE('',#4012);
#377=PLANE('',#4016);
#378=PLANE('',#4020);
#379=PLANE('',#4024);
#380=PLANE('',#4029);
#381=PLANE('',#4031);
#382=PLANE('',#4041);
#383=PLANE('',#4045);
#384=PLANE('',#4049);
#385=PLANE('',#4053);
#386=PLANE('',#4057);
#387=PLANE('',#4061);
#388=PLANE('',#4065);
#389=PLANE('',#4066);
#517=FACE_OUTER_BOUND('',#758,.T.);
#518=FACE_OUTER_BOUND('',#759,.T.);
#519=FACE_OUTER_BOUND('',#760,.T.);
#520=FACE_OUTER_BOUND('',#761,.T.);
#521=FACE_OUTER_BOUND('',#762,.T.);
#522=FACE_OUTER_BOUND('',#763,.T.);
#523=FACE_OUTER_BOUND('',#764,.T.);
#524=FACE_OUTER_BOUND('',#765,.T.);
#525=FACE_OUTER_BOUND('',#766,.T.);
#526=FACE_OUTER_BOUND('',#767,.T.);
#527=FACE_OUTER_BOUND('',#768,.T.);
#528=FACE_OUTER_BOUND('',#769,.T.);
#529=FACE_OUTER_BOUND('',#770,.T.);
#530=FACE_OUTER_BOUND('',#771,.T.);
#531=FACE_OUTER_BOUND('',#772,.T.);
#532=FACE_OUTER_BOUND('',#773,.T.);
#533=FACE_OUTER_BOUND('',#774,.T.);
#534=FACE_OUTER_BOUND('',#775,.T.);
#535=FACE_OUTER_BOUND('',#776,.T.);
#536=FACE_OUTER_BOUND('',#777,.T.);
#537=FACE_OUTER_BOUND('',#778,.T.);
#538=FACE_OUTER_BOUND('',#780,.T.);
#539=FACE_OUTER_BOUND('',#781,.T.);
#540=FACE_OUTER_BOUND('',#782,.T.);
#541=FACE_OUTER_BOUND('',#783,.T.);
#542=FACE_OUTER_BOUND('',#784,.T.);
#543=FACE_OUTER_BOUND('',#785,.T.);
#544=FACE_OUTER_BOUND('',#786,.T.);
#545=FACE_OUTER_BOUND('',#787,.T.);
#546=FACE_OUTER_BOUND('',#789,.T.);
#547=FACE_OUTER_BOUND('',#790,.T.);
#548=FACE_OUTER_BOUND('',#792,.T.);
#549=FACE_OUTER_BOUND('',#794,.T.);
#550=FACE_OUTER_BOUND('',#802,.T.);
#758=EDGE_LOOP('',(#2554,#2555,#2556,#2557));
#759=EDGE_LOOP('',(#2558));
#760=EDGE_LOOP('',(#2559,#2560,#2561,#2562));
#761=EDGE_LOOP('',(#2563));
#762=EDGE_LOOP('',(#2564,#2565,#2566,#2567));
#763=EDGE_LOOP('',(#2568));
#764=EDGE_LOOP('',(#2569,#2570,#2571,#2572));
#765=EDGE_LOOP('',(#2573));
#766=EDGE_LOOP('',(#2574,#2575,#2576,#2577));
#767=EDGE_LOOP('',(#2578));
#768=EDGE_LOOP('',(#2579,#2580,#2581,#2582));
#769=EDGE_LOOP('',(#2583));
#770=EDGE_LOOP('',(#2584,#2585));
#771=EDGE_LOOP('',(#2586,#2587));
#772=EDGE_LOOP('',(#2588,#2589,#2590,#2591));
#773=EDGE_LOOP('',(#2592,#2593,#2594,#2595));
#774=EDGE_LOOP('',(#2596,#2597,#2598,#2599,#2600,#2601));
#775=EDGE_LOOP('',(#2602,#2603,#2604,#2605,#2606,#2607,#2608));
#776=EDGE_LOOP('',(#2609,#2610,#2611,#2612,#2613,#2614));
#777=EDGE_LOOP('',(#2615,#2616,#2617,#2618,#2619,#2620));
#778=EDGE_LOOP('',(#2621));
#779=EDGE_LOOP('',(#2622));
#780=EDGE_LOOP('',(#2623,#2624,#2625,#2626));
#781=EDGE_LOOP('',(#2627));
#782=EDGE_LOOP('',(#2628,#2629,#2630,#2631));
#783=EDGE_LOOP('',(#2632));
#784=EDGE_LOOP('',(#2633,#2634,#2635,#2636));
#785=EDGE_LOOP('',(#2637,#2638,#2639,#2640));
#786=EDGE_LOOP('',(#2641,#2642,#2643,#2644));
#787=EDGE_LOOP('',(#2645));
#788=EDGE_LOOP('',(#2646));
#789=EDGE_LOOP('',(#2647,#2648,#2649,#2650,#2651,#2652,#2653,#2654,#2655,
#2656,#2657,#2658));
#790=EDGE_LOOP('',(#2659));
#791=EDGE_LOOP('',(#2660));
#792=EDGE_LOOP('',(#2661,#2662,#2663,#2664,#2665,#2666,#2667,#2668,#2669));
#793=EDGE_LOOP('',(#2670,#2671));
#794=EDGE_LOOP('',(#2672));
#795=EDGE_LOOP('',(#2673));
#796=EDGE_LOOP('',(#2674));
#797=EDGE_LOOP('',(#2675));
#798=EDGE_LOOP('',(#2676));
#799=EDGE_LOOP('',(#2677));
#800=EDGE_LOOP('',(#2678));
#801=EDGE_LOOP('',(#2679));
#802=EDGE_LOOP('',(#2680));
#803=EDGE_LOOP('',(#2681));
#804=EDGE_LOOP('',(#2682));
#805=EDGE_LOOP('',(#2683));
#1082=LINE('',#5731,#1326);
#1083=LINE('',#5738,#1327);
#1084=LINE('',#5745,#1328);
#1085=LINE('',#5752,#1329);
#1086=LINE('',#5759,#1330);
#1087=LINE('',#5766,#1331);
#1088=LINE('',#5814,#1332);
#1089=LINE('',#5817,#1333);
#1090=LINE('',#5819,#1334);
#1091=LINE('',#5821,#1335);
#1092=LINE('',#5824,#1336);
#1093=LINE('',#5866,#1337);
#1094=LINE('',#5887,#1338);
#1095=LINE('',#5888,#1339);
#1096=LINE('',#5911,#1340);
#1097=LINE('',#5956,#1341);
#1098=LINE('',#5963,#1342);
#1099=LINE('',#5970,#1343);
#1100=LINE('',#5976,#1344);
#1101=LINE('',#5983,#1345);
#1102=LINE('',#5989,#1346);
#1103=LINE('',#5991,#1347);
#1104=LINE('',#5997,#1348);
#1105=LINE('',#5999,#1349);
#1326=VECTOR('',#4550,0.21);
#1327=VECTOR('',#4559,0.21);
#1328=VECTOR('',#4568,0.21);
#1329=VECTOR('',#4577,0.21);
#1330=VECTOR('',#4586,0.21);
#1331=VECTOR('',#4595,0.21);
#1332=VECTOR('',#4610,1.);
#1333=VECTOR('',#4613,1.);
#1334=VECTOR('',#4616,1.);
#1335=VECTOR('',#4619,1.);
#1336=VECTOR('',#4622,0.685);
#1337=VECTOR('',#4627,0.4);
#1338=VECTOR('',#4628,1.);
#1339=VECTOR('',#4629,1.);
#1340=VECTOR('',#4634,0.8);
#1341=VECTOR('',#4639,0.685);
#1342=VECTOR('',#4648,0.165);
#1343=VECTOR('',#4657,0.165);
#1344=VECTOR('',#4666,0.925);
#1345=VECTOR('',#4675,0.6);
#1346=VECTOR('',#4684,2.5);
#1347=VECTOR('',#4685,2.5);
#1348=VECTOR('',#4694,4.);
#1349=VECTOR('',#4695,4.);
#1538=CIRCLE('',#4002,0.21);
#1539=CIRCLE('',#4003,0.21);
#1540=CIRCLE('',#4006,0.21);
#1541=CIRCLE('',#4007,0.21);
#1542=CIRCLE('',#4010,0.21);
#1543=CIRCLE('',#4011,0.21);
#1544=CIRCLE('',#4014,0.21);
#1545=CIRCLE('',#4015,0.21);
#1546=CIRCLE('',#4018,0.21);
#1547=CIRCLE('',#4019,0.21);
#1548=CIRCLE('',#4022,0.21);
#1549=CIRCLE('',#4023,0.21);
#1550=CIRCLE('',#4026,0.4);
#1551=CIRCLE('',#4028,0.4);
#1552=CIRCLE('',#4030,0.685);
#1553=CIRCLE('',#4032,0.685);
#1554=CIRCLE('',#4035,0.4);
#1555=CIRCLE('',#4037,0.8);
#1556=CIRCLE('',#4038,0.8);
#1557=CIRCLE('',#4040,0.685);
#1558=CIRCLE('',#4043,0.165);
#1559=CIRCLE('',#4044,0.165);
#1560=CIRCLE('',#4047,0.165);
#1561=CIRCLE('',#4048,0.165);
#1562=CIRCLE('',#4051,0.925);
#1563=CIRCLE('',#4052,0.925);
#1564=CIRCLE('',#4055,0.6);
#1565=CIRCLE('',#4056,0.6);
#1566=CIRCLE('',#4059,2.5);
#1567=CIRCLE('',#4060,2.5);
#1568=CIRCLE('',#4063,4.);
#1569=CIRCLE('',#4064,4.);
#1745=VERTEX_POINT('',#5728);
#1746=VERTEX_POINT('',#5730);
#1747=VERTEX_POINT('',#5735);
#1748=VERTEX_POINT('',#5737);
#1749=VERTEX_POINT('',#5742);
#1750=VERTEX_POINT('',#5744);
#1751=VERTEX_POINT('',#5749);
#1752=VERTEX_POINT('',#5751);
#1753=VERTEX_POINT('',#5756);
#1754=VERTEX_POINT('',#5758);
#1755=VERTEX_POINT('',#5763);
#1756=VERTEX_POINT('',#5765);
#1757=VERTEX_POINT('',#5770);
#1758=VERTEX_POINT('',#5771);
#1759=VERTEX_POINT('',#5813);
#1760=VERTEX_POINT('',#5815);
#1761=VERTEX_POINT('',#5823);
#1762=VERTEX_POINT('',#5825);
#1763=VERTEX_POINT('',#5863);
#1764=VERTEX_POINT('',#5865);
#1765=VERTEX_POINT('',#5867);
#1766=VERTEX_POINT('',#5886);
#1767=VERTEX_POINT('',#5910);
#1768=VERTEX_POINT('',#5914);
#1769=VERTEX_POINT('',#5915);
#1770=VERTEX_POINT('',#5926);
#1771=VERTEX_POINT('',#5955);
#1772=VERTEX_POINT('',#5960);
#1773=VERTEX_POINT('',#5962);
#1774=VERTEX_POINT('',#5967);
#1775=VERTEX_POINT('',#5969);
#1776=VERTEX_POINT('',#5974);
#1777=VERTEX_POINT('',#5980);
#1778=VERTEX_POINT('',#5982);
#1779=VERTEX_POINT('',#5987);
#1780=VERTEX_POINT('',#5990);
#1781=VERTEX_POINT('',#5995);
#1782=VERTEX_POINT('',#5998);
#2053=EDGE_CURVE('',#1745,#1745,#1538,.T.);
#2054=EDGE_CURVE('',#1745,#1746,#1082,.T.);
#2055=EDGE_CURVE('',#1746,#1746,#1539,.T.);
#2056=EDGE_CURVE('',#1747,#1747,#1540,.T.);
#2057=EDGE_CURVE('',#1747,#1748,#1083,.T.);
#2058=EDGE_CURVE('',#1748,#1748,#1541,.T.);
#2059=EDGE_CURVE('',#1749,#1749,#1542,.T.);
#2060=EDGE_CURVE('',#1749,#1750,#1084,.T.);
#2061=EDGE_CURVE('',#1750,#1750,#1543,.T.);
#2062=EDGE_CURVE('',#1751,#1751,#1544,.T.);
#2063=EDGE_CURVE('',#1751,#1752,#1085,.T.);
#2064=EDGE_CURVE('',#1752,#1752,#1545,.T.);
#2065=EDGE_CURVE('',#1753,#1753,#1546,.T.);
#2066=EDGE_CURVE('',#1753,#1754,#1086,.T.);
#2067=EDGE_CURVE('',#1754,#1754,#1547,.T.);
#2068=EDGE_CURVE('',#1755,#1755,#1548,.T.);
#2069=EDGE_CURVE('',#1755,#1756,#1087,.T.);
#2070=EDGE_CURVE('',#1756,#1756,#1549,.T.);
#2071=EDGE_CURVE('',#1757,#1758,#1550,.T.);
#2072=EDGE_CURVE('',#1758,#1757,#167,.T.);
#2073=EDGE_CURVE('',#1758,#1757,#1551,.T.);
#2074=EDGE_CURVE('',#1757,#1758,#168,.T.);
#2075=EDGE_CURVE('',#1759,#1758,#1088,.T.);
#2076=EDGE_CURVE('',#1759,#1760,#1552,.T.);
#2077=EDGE_CURVE('',#1757,#1760,#1089,.T.);
#2078=EDGE_CURVE('',#1757,#1760,#1090,.T.);
#2079=EDGE_CURVE('',#1760,#1759,#1553,.T.);
#2080=EDGE_CURVE('',#1759,#1758,#1091,.T.);
#2081=EDGE_CURVE('',#1759,#1761,#1092,.T.);
#2082=EDGE_CURVE('',#1762,#1761,#169,.T.);
#2083=EDGE_CURVE('',#1761,#1762,#170,.T.);
#2084=EDGE_CURVE('',#1763,#1763,#1554,.T.);
#2085=EDGE_CURVE('',#1763,#1764,#1093,.T.);
#2086=EDGE_CURVE('',#1765,#1764,#171,.T.);
#2087=EDGE_CURVE('',#1766,#1765,#1094,.T.);
#2088=EDGE_CURVE('',#1766,#1765,#1095,.T.);
#2089=EDGE_CURVE('',#1764,#1765,#172,.T.);
#2090=EDGE_CURVE('',#1765,#1765,#1555,.T.);
#2091=EDGE_CURVE('',#1764,#1767,#1096,.T.);
#2092=EDGE_CURVE('',#1767,#1767,#1556,.T.);
#2093=EDGE_CURVE('',#1768,#1769,#173,.T.);
#2094=EDGE_CURVE('',#1770,#1768,#174,.T.);
#2095=EDGE_CURVE('',#1769,#1770,#175,.T.);
#2096=EDGE_CURVE('',#1769,#1771,#1097,.T.);
#2097=EDGE_CURVE('',#1771,#1771,#1557,.T.);
#2098=EDGE_CURVE('',#1772,#1772,#1558,.T.);
#2099=EDGE_CURVE('',#1772,#1773,#1098,.T.);
#2100=EDGE_CURVE('',#1773,#1773,#1559,.T.);
#2101=EDGE_CURVE('',#1774,#1774,#1560,.T.);
#2102=EDGE_CURVE('',#1774,#1775,#1099,.T.);
#2103=EDGE_CURVE('',#1775,#1775,#1561,.T.);
#2104=EDGE_CURVE('',#1776,#1776,#1562,.T.);
#2105=EDGE_CURVE('',#1776,#1766,#1100,.T.);
#2106=EDGE_CURVE('',#1766,#1766,#1563,.T.);
#2107=EDGE_CURVE('',#1777,#1777,#1564,.T.);
#2108=EDGE_CURVE('',#1777,#1778,#1101,.T.);
#2109=EDGE_CURVE('',#1778,#1778,#1565,.T.);
#2110=EDGE_CURVE('',#1779,#1779,#1566,.T.);
#2111=EDGE_CURVE('',#1779,#1760,#1102,.T.);
#2112=EDGE_CURVE('',#1759,#1780,#1103,.T.);
#2113=EDGE_CURVE('',#1780,#1780,#1567,.T.);
#2114=EDGE_CURVE('',#1781,#1781,#1568,.T.);
#2115=EDGE_CURVE('',#1781,#1769,#1104,.T.);
#2116=EDGE_CURVE('',#1770,#1782,#1105,.T.);
#2117=EDGE_CURVE('',#1782,#1782,#1569,.T.);
#2554=ORIENTED_EDGE('',*,*,#2053,.F.);
#2555=ORIENTED_EDGE('',*,*,#2054,.T.);
#2556=ORIENTED_EDGE('',*,*,#2055,.F.);
#2557=ORIENTED_EDGE('',*,*,#2054,.F.);
#2558=ORIENTED_EDGE('',*,*,#2053,.T.);
#2559=ORIENTED_EDGE('',*,*,#2056,.F.);
#2560=ORIENTED_EDGE('',*,*,#2057,.T.);
#2561=ORIENTED_EDGE('',*,*,#2058,.F.);
#2562=ORIENTED_EDGE('',*,*,#2057,.F.);
#2563=ORIENTED_EDGE('',*,*,#2056,.T.);
#2564=ORIENTED_EDGE('',*,*,#2059,.F.);
#2565=ORIENTED_EDGE('',*,*,#2060,.T.);
#2566=ORIENTED_EDGE('',*,*,#2061,.F.);
#2567=ORIENTED_EDGE('',*,*,#2060,.F.);
#2568=ORIENTED_EDGE('',*,*,#2059,.T.);
#2569=ORIENTED_EDGE('',*,*,#2062,.F.);
#2570=ORIENTED_EDGE('',*,*,#2063,.T.);
#2571=ORIENTED_EDGE('',*,*,#2064,.F.);
#2572=ORIENTED_EDGE('',*,*,#2063,.F.);
#2573=ORIENTED_EDGE('',*,*,#2062,.T.);
#2574=ORIENTED_EDGE('',*,*,#2065,.F.);
#2575=ORIENTED_EDGE('',*,*,#2066,.T.);
#2576=ORIENTED_EDGE('',*,*,#2067,.F.);
#2577=ORIENTED_EDGE('',*,*,#2066,.F.);
#2578=ORIENTED_EDGE('',*,*,#2065,.T.);
#2579=ORIENTED_EDGE('',*,*,#2068,.F.);
#2580=ORIENTED_EDGE('',*,*,#2069,.T.);
#2581=ORIENTED_EDGE('',*,*,#2070,.F.);
#2582=ORIENTED_EDGE('',*,*,#2069,.F.);
#2583=ORIENTED_EDGE('',*,*,#2068,.T.);
#2584=ORIENTED_EDGE('',*,*,#2071,.F.);
#2585=ORIENTED_EDGE('',*,*,#2072,.F.);
#2586=ORIENTED_EDGE('',*,*,#2073,.F.);
#2587=ORIENTED_EDGE('',*,*,#2074,.F.);
#2588=ORIENTED_EDGE('',*,*,#2071,.T.);
#2589=ORIENTED_EDGE('',*,*,#2075,.F.);
#2590=ORIENTED_EDGE('',*,*,#2076,.T.);
#2591=ORIENTED_EDGE('',*,*,#2077,.F.);
#2592=ORIENTED_EDGE('',*,*,#2073,.T.);
#2593=ORIENTED_EDGE('',*,*,#2078,.T.);
#2594=ORIENTED_EDGE('',*,*,#2079,.T.);
#2595=ORIENTED_EDGE('',*,*,#2080,.T.);
#2596=ORIENTED_EDGE('',*,*,#2076,.F.);
#2597=ORIENTED_EDGE('',*,*,#2081,.T.);
#2598=ORIENTED_EDGE('',*,*,#2082,.F.);
#2599=ORIENTED_EDGE('',*,*,#2083,.F.);
#2600=ORIENTED_EDGE('',*,*,#2081,.F.);
#2601=ORIENTED_EDGE('',*,*,#2079,.F.);
#2602=ORIENTED_EDGE('',*,*,#2084,.F.);
#2603=ORIENTED_EDGE('',*,*,#2085,.T.);
#2604=ORIENTED_EDGE('',*,*,#2086,.F.);
#2605=ORIENTED_EDGE('',*,*,#2087,.F.);
#2606=ORIENTED_EDGE('',*,*,#2088,.T.);
#2607=ORIENTED_EDGE('',*,*,#2089,.F.);
#2608=ORIENTED_EDGE('',*,*,#2085,.F.);
#2609=ORIENTED_EDGE('',*,*,#2090,.T.);
#2610=ORIENTED_EDGE('',*,*,#2086,.T.);
#2611=ORIENTED_EDGE('',*,*,#2091,.T.);
#2612=ORIENTED_EDGE('',*,*,#2092,.T.);
#2613=ORIENTED_EDGE('',*,*,#2091,.F.);
#2614=ORIENTED_EDGE('',*,*,#2089,.T.);
#2615=ORIENTED_EDGE('',*,*,#2093,.F.);
#2616=ORIENTED_EDGE('',*,*,#2094,.F.);
#2617=ORIENTED_EDGE('',*,*,#2095,.F.);
#2618=ORIENTED_EDGE('',*,*,#2096,.T.);
#2619=ORIENTED_EDGE('',*,*,#2097,.T.);
#2620=ORIENTED_EDGE('',*,*,#2096,.F.);
#2621=ORIENTED_EDGE('',*,*,#2097,.F.);
#2622=ORIENTED_EDGE('',*,*,#2084,.T.);
#2623=ORIENTED_EDGE('',*,*,#2098,.F.);
#2624=ORIENTED_EDGE('',*,*,#2099,.T.);
#2625=ORIENTED_EDGE('',*,*,#2100,.T.);
#2626=ORIENTED_EDGE('',*,*,#2099,.F.);
#2627=ORIENTED_EDGE('',*,*,#2100,.F.);
#2628=ORIENTED_EDGE('',*,*,#2101,.F.);
#2629=ORIENTED_EDGE('',*,*,#2102,.T.);
#2630=ORIENTED_EDGE('',*,*,#2103,.T.);
#2631=ORIENTED_EDGE('',*,*,#2102,.F.);
#2632=ORIENTED_EDGE('',*,*,#2103,.F.);
#2633=ORIENTED_EDGE('',*,*,#2104,.F.);
#2634=ORIENTED_EDGE('',*,*,#2105,.T.);
#2635=ORIENTED_EDGE('',*,*,#2106,.T.);
#2636=ORIENTED_EDGE('',*,*,#2105,.F.);
#2637=ORIENTED_EDGE('',*,*,#2106,.F.);
#2638=ORIENTED_EDGE('',*,*,#2087,.T.);
#2639=ORIENTED_EDGE('',*,*,#2090,.F.);
#2640=ORIENTED_EDGE('',*,*,#2088,.F.);
#2641=ORIENTED_EDGE('',*,*,#2107,.F.);
#2642=ORIENTED_EDGE('',*,*,#2108,.T.);
#2643=ORIENTED_EDGE('',*,*,#2109,.F.);
#2644=ORIENTED_EDGE('',*,*,#2108,.F.);
#2645=ORIENTED_EDGE('',*,*,#2092,.F.);
#2646=ORIENTED_EDGE('',*,*,#2107,.T.);
#2647=ORIENTED_EDGE('',*,*,#2110,.F.);
#2648=ORIENTED_EDGE('',*,*,#2111,.T.);
#2649=ORIENTED_EDGE('',*,*,#2078,.F.);
#2650=ORIENTED_EDGE('',*,*,#2074,.T.);
#2651=ORIENTED_EDGE('',*,*,#2080,.F.);
#2652=ORIENTED_EDGE('',*,*,#2112,.T.);
#2653=ORIENTED_EDGE('',*,*,#2113,.F.);
#2654=ORIENTED_EDGE('',*,*,#2112,.F.);
#2655=ORIENTED_EDGE('',*,*,#2075,.T.);
#2656=ORIENTED_EDGE('',*,*,#2072,.T.);
#2657=ORIENTED_EDGE('',*,*,#2077,.T.);
#2658=ORIENTED_EDGE('',*,*,#2111,.F.);
#2659=ORIENTED_EDGE('',*,*,#2110,.T.);
#2660=ORIENTED_EDGE('',*,*,#2109,.T.);
#2661=ORIENTED_EDGE('',*,*,#2114,.F.);
#2662=ORIENTED_EDGE('',*,*,#2115,.T.);
#2663=ORIENTED_EDGE('',*,*,#2095,.T.);
#2664=ORIENTED_EDGE('',*,*,#2116,.T.);
#2665=ORIENTED_EDGE('',*,*,#2117,.T.);
#2666=ORIENTED_EDGE('',*,*,#2116,.F.);
#2667=ORIENTED_EDGE('',*,*,#2094,.T.);
#2668=ORIENTED_EDGE('',*,*,#2093,.T.);
#2669=ORIENTED_EDGE('',*,*,#2115,.F.);
#2670=ORIENTED_EDGE('',*,*,#2082,.T.);
#2671=ORIENTED_EDGE('',*,*,#2083,.T.);
#2672=ORIENTED_EDGE('',*,*,#2114,.T.);
#2673=ORIENTED_EDGE('',*,*,#2113,.T.);
#2674=ORIENTED_EDGE('',*,*,#2070,.T.);
#2675=ORIENTED_EDGE('',*,*,#2067,.T.);
#2676=ORIENTED_EDGE('',*,*,#2064,.T.);
#2677=ORIENTED_EDGE('',*,*,#2061,.T.);
#2678=ORIENTED_EDGE('',*,*,#2058,.T.);
#2679=ORIENTED_EDGE('',*,*,#2055,.T.);
#2680=ORIENTED_EDGE('',*,*,#2117,.F.);
#2681=ORIENTED_EDGE('',*,*,#2098,.T.);
#2682=ORIENTED_EDGE('',*,*,#2101,.T.);
#2683=ORIENTED_EDGE('',*,*,#2104,.T.);
#3368=CYLINDRICAL_SURFACE('',#4001,0.21);
#3369=CYLINDRICAL_SURFACE('',#4005,0.21);
#3370=CYLINDRICAL_SURFACE('',#4009,0.21);
#3371=CYLINDRICAL_SURFACE('',#4013,0.21);
#3372=CYLINDRICAL_SURFACE('',#4017,0.21);
#3373=CYLINDRICAL_SURFACE('',#4021,0.21);
#3374=CYLINDRICAL_SURFACE('',#4025,0.4);
#3375=CYLINDRICAL_SURFACE('',#4027,0.4);
#3376=CYLINDRICAL_SURFACE('',#4033,0.685);
#3377=CYLINDRICAL_SURFACE('',#4034,0.4);
#3378=CYLINDRICAL_SURFACE('',#4036,0.8);
#3379=CYLINDRICAL_SURFACE('',#4039,0.685);
#3380=CYLINDRICAL_SURFACE('',#4042,0.165);
#3381=CYLINDRICAL_SURFACE('',#4046,0.165);
#3382=CYLINDRICAL_SURFACE('',#4050,0.925);
#3383=CYLINDRICAL_SURFACE('',#4054,0.6);
#3384=CYLINDRICAL_SURFACE('',#4058,2.5);
#3385=CYLINDRICAL_SURFACE('',#4062,4.);
#3464=ADVANCED_FACE('',(#517),#3368,.F.);
#3465=ADVANCED_FACE('',(#518),#374,.T.);
#3466=ADVANCED_FACE('',(#519),#3369,.F.);
#3467=ADVANCED_FACE('',(#520),#375,.T.);
#3468=ADVANCED_FACE('',(#521),#3370,.F.);
#3469=ADVANCED_FACE('',(#522),#376,.T.);
#3470=ADVANCED_FACE('',(#523),#3371,.F.);
#3471=ADVANCED_FACE('',(#524),#377,.T.);
#3472=ADVANCED_FACE('',(#525),#3372,.F.);
#3473=ADVANCED_FACE('',(#526),#378,.T.);
#3474=ADVANCED_FACE('',(#527),#3373,.F.);
#3475=ADVANCED_FACE('',(#528),#379,.T.);
#3476=ADVANCED_FACE('',(#529),#3374,.F.);
#3477=ADVANCED_FACE('',(#530),#3375,.F.);
#3478=ADVANCED_FACE('',(#531),#380,.T.);
#3479=ADVANCED_FACE('',(#532),#381,.T.);
#3480=ADVANCED_FACE('',(#533),#3376,.F.);
#3481=ADVANCED_FACE('',(#534),#3377,.F.);
#3482=ADVANCED_FACE('',(#535),#3378,.F.);
#3483=ADVANCED_FACE('',(#536),#3379,.F.);
#3484=ADVANCED_FACE('',(#537,#283),#382,.F.);
#3485=ADVANCED_FACE('',(#538),#3380,.F.);
#3486=ADVANCED_FACE('',(#539),#383,.F.);
#3487=ADVANCED_FACE('',(#540),#3381,.F.);
#3488=ADVANCED_FACE('',(#541),#384,.F.);
#3489=ADVANCED_FACE('',(#542),#3382,.F.);
#3490=ADVANCED_FACE('',(#543),#385,.F.);
#3491=ADVANCED_FACE('',(#544),#3383,.F.);
#3492=ADVANCED_FACE('',(#545,#284),#386,.F.);
#3493=ADVANCED_FACE('',(#546),#3384,.F.);
#3494=ADVANCED_FACE('',(#547,#285),#387,.T.);
#3495=ADVANCED_FACE('',(#548,#286),#3385,.T.);
#3496=ADVANCED_FACE('',(#549,#287,#288,#289,#290,#291,#292,#293),#388,.T.);
#3497=ADVANCED_FACE('',(#550,#294,#295,#296),#389,.F.);
#3678=CLOSED_SHELL('',(#3464,#3465,#3466,#3467,#3468,#3469,#3470,#3471,
#3472,#3473,#3474,#3475,#3476,#3477,#3478,#3479,#3480,#3481,#3482,#3483,
#3484,#3485,#3486,#3487,#3488,#3489,#3490,#3491,#3492,#3493,#3494,#3495,
#3496,#3497));
#4000=AXIS2_PLACEMENT_3D('',#5726,#4544,#4545);
#4001=AXIS2_PLACEMENT_3D('',#5727,#4546,#4547);
#4002=AXIS2_PLACEMENT_3D('',#5729,#4548,#4549);
#4003=AXIS2_PLACEMENT_3D('',#5732,#4551,#4552);
#4004=AXIS2_PLACEMENT_3D('',#5733,#4553,#4554);
#4005=AXIS2_PLACEMENT_3D('',#5734,#4555,#4556);
#4006=AXIS2_PLACEMENT_3D('',#5736,#4557,#4558);
#4007=AXIS2_PLACEMENT_3D('',#5739,#4560,#4561);
#4008=AXIS2_PLACEMENT_3D('',#5740,#4562,#4563);
#4009=AXIS2_PLACEMENT_3D('',#5741,#4564,#4565);
#4010=AXIS2_PLACEMENT_3D('',#5743,#4566,#4567);
#4011=AXIS2_PLACEMENT_3D('',#5746,#4569,#4570);
#4012=AXIS2_PLACEMENT_3D('',#5747,#4571,#4572);
#4013=AXIS2_PLACEMENT_3D('',#5748,#4573,#4574);
#4014=AXIS2_PLACEMENT_3D('',#5750,#4575,#4576);
#4015=AXIS2_PLACEMENT_3D('',#5753,#4578,#4579);
#4016=AXIS2_PLACEMENT_3D('',#5754,#4580,#4581);
#4017=AXIS2_PLACEMENT_3D('',#5755,#4582,#4583);
#4018=AXIS2_PLACEMENT_3D('',#5757,#4584,#4585);
#4019=AXIS2_PLACEMENT_3D('',#5760,#4587,#4588);
#4020=AXIS2_PLACEMENT_3D('',#5761,#4589,#4590);
#4021=AXIS2_PLACEMENT_3D('',#5762,#4591,#4592);
#4022=AXIS2_PLACEMENT_3D('',#5764,#4593,#4594);
#4023=AXIS2_PLACEMENT_3D('',#5767,#4596,#4597);
#4024=AXIS2_PLACEMENT_3D('',#5768,#4598,#4599);
#4025=AXIS2_PLACEMENT_3D('',#5769,#4600,#4601);
#4026=AXIS2_PLACEMENT_3D('',#5772,#4602,#4603);
#4027=AXIS2_PLACEMENT_3D('',#5791,#4604,#4605);
#4028=AXIS2_PLACEMENT_3D('',#5792,#4606,#4607);
#4029=AXIS2_PLACEMENT_3D('',#5812,#4608,#4609);
#4030=AXIS2_PLACEMENT_3D('',#5816,#4611,#4612);
#4031=AXIS2_PLACEMENT_3D('',#5818,#4614,#4615);
#4032=AXIS2_PLACEMENT_3D('',#5820,#4617,#4618);
#4033=AXIS2_PLACEMENT_3D('',#5822,#4620,#4621);
#4034=AXIS2_PLACEMENT_3D('',#5862,#4623,#4624);
#4035=AXIS2_PLACEMENT_3D('',#5864,#4625,#4626);
#4036=AXIS2_PLACEMENT_3D('',#5908,#4630,#4631);
#4037=AXIS2_PLACEMENT_3D('',#5909,#4632,#4633);
#4038=AXIS2_PLACEMENT_3D('',#5912,#4635,#4636);
#4039=AXIS2_PLACEMENT_3D('',#5913,#4637,#4638);
#4040=AXIS2_PLACEMENT_3D('',#5957,#4640,#4641);
#4041=AXIS2_PLACEMENT_3D('',#5958,#4642,#4643);
#4042=AXIS2_PLACEMENT_3D('',#5959,#4644,#4645);
#4043=AXIS2_PLACEMENT_3D('',#5961,#4646,#4647);
#4044=AXIS2_PLACEMENT_3D('',#5964,#4649,#4650);
#4045=AXIS2_PLACEMENT_3D('',#5965,#4651,#4652);
#4046=AXIS2_PLACEMENT_3D('',#5966,#4653,#4654);
#4047=AXIS2_PLACEMENT_3D('',#5968,#4655,#4656);
#4048=AXIS2_PLACEMENT_3D('',#5971,#4658,#4659);
#4049=AXIS2_PLACEMENT_3D('',#5972,#4660,#4661);
#4050=AXIS2_PLACEMENT_3D('',#5973,#4662,#4663);
#4051=AXIS2_PLACEMENT_3D('',#5975,#4664,#4665);
#4052=AXIS2_PLACEMENT_3D('',#5977,#4667,#4668);
#4053=AXIS2_PLACEMENT_3D('',#5978,#4669,#4670);
#4054=AXIS2_PLACEMENT_3D('',#5979,#4671,#4672);
#4055=AXIS2_PLACEMENT_3D('',#5981,#4673,#4674);
#4056=AXIS2_PLACEMENT_3D('',#5984,#4676,#4677);
#4057=AXIS2_PLACEMENT_3D('',#5985,#4678,#4679);
#4058=AXIS2_PLACEMENT_3D('',#5986,#4680,#4681);
#4059=AXIS2_PLACEMENT_3D('',#5988,#4682,#4683);
#4060=AXIS2_PLACEMENT_3D('',#5992,#4686,#4687);
#4061=AXIS2_PLACEMENT_3D('',#5993,#4688,#4689);
#4062=AXIS2_PLACEMENT_3D('',#5994,#4690,#4691);
#4063=AXIS2_PLACEMENT_3D('',#5996,#4692,#4693);
#4064=AXIS2_PLACEMENT_3D('',#6000,#4696,#4697);
#4065=AXIS2_PLACEMENT_3D('',#6001,#4698,#4699);
#4066=AXIS2_PLACEMENT_3D('',#6002,#4700,#4701);
#4544=DIRECTION('axis',(0.,0.,1.));
#4545=DIRECTION('refdir',(1.,0.,0.));
#4546=DIRECTION('center_axis',(0.,0.,1.));
#4547=DIRECTION('ref_axis',(1.,0.,0.));
#4548=DIRECTION('center_axis',(0.,0.,1.));
#4549=DIRECTION('ref_axis',(1.,0.,0.));
#4550=DIRECTION('',(0.,0.,1.));
#4551=DIRECTION('center_axis',(0.,0.,-1.));
#4552=DIRECTION('ref_axis',(1.,0.,0.));
#4553=DIRECTION('center_axis',(0.,0.,1.));
#4554=DIRECTION('ref_axis',(1.,0.,0.));
#4555=DIRECTION('center_axis',(0.,0.,1.));
#4556=DIRECTION('ref_axis',(1.,0.,0.));
#4557=DIRECTION('center_axis',(0.,0.,1.));
#4558=DIRECTION('ref_axis',(1.,0.,0.));
#4559=DIRECTION('',(0.,0.,1.));
#4560=DIRECTION('center_axis',(0.,0.,-1.));
#4561=DIRECTION('ref_axis',(1.,0.,0.));
#4562=DIRECTION('center_axis',(0.,0.,1.));
#4563=DIRECTION('ref_axis',(1.,0.,0.));
#4564=DIRECTION('center_axis',(0.,0.,1.));
#4565=DIRECTION('ref_axis',(1.,0.,0.));
#4566=DIRECTION('center_axis',(0.,0.,1.));
#4567=DIRECTION('ref_axis',(1.,0.,0.));
#4568=DIRECTION('',(0.,0.,1.));
#4569=DIRECTION('center_axis',(0.,0.,-1.));
#4570=DIRECTION('ref_axis',(1.,0.,0.));
#4571=DIRECTION('center_axis',(0.,0.,1.));
#4572=DIRECTION('ref_axis',(1.,0.,0.));
#4573=DIRECTION('center_axis',(0.,0.,1.));
#4574=DIRECTION('ref_axis',(1.,0.,0.));
#4575=DIRECTION('center_axis',(0.,0.,1.));
#4576=DIRECTION('ref_axis',(1.,0.,0.));
#4577=DIRECTION('',(0.,0.,1.));
#4578=DIRECTION('center_axis',(0.,0.,-1.));
#4579=DIRECTION('ref_axis',(1.,0.,0.));
#4580=DIRECTION('center_axis',(0.,0.,1.));
#4581=DIRECTION('ref_axis',(1.,0.,0.));
#4582=DIRECTION('center_axis',(0.,0.,1.));
#4583=DIRECTION('ref_axis',(1.,0.,0.));
#4584=DIRECTION('center_axis',(0.,0.,1.));
#4585=DIRECTION('ref_axis',(1.,0.,0.));
#4586=DIRECTION('',(0.,0.,1.));
#4587=DIRECTION('center_axis',(0.,0.,-1.));
#4588=DIRECTION('ref_axis',(1.,0.,0.));
#4589=DIRECTION('center_axis',(0.,0.,1.));
#4590=DIRECTION('ref_axis',(1.,0.,0.));
#4591=DIRECTION('center_axis',(0.,0.,1.));
#4592=DIRECTION('ref_axis',(1.,0.,0.));
#4593=DIRECTION('center_axis',(0.,0.,1.));
#4594=DIRECTION('ref_axis',(1.,0.,0.));
#4595=DIRECTION('',(0.,0.,1.));
#4596=DIRECTION('center_axis',(0.,0.,-1.));
#4597=DIRECTION('ref_axis',(1.,0.,0.));
#4598=DIRECTION('center_axis',(0.,0.,1.));
#4599=DIRECTION('ref_axis',(1.,0.,0.));
#4600=DIRECTION('center_axis',(1.,0.,0.));
#4601=DIRECTION('ref_axis',(0.,0.,-1.));
#4602=DIRECTION('center_axis',(-1.,0.,0.));
#4603=DIRECTION('ref_axis',(0.,0.,-1.));
#4604=DIRECTION('center_axis',(1.,0.,0.));
#4605=DIRECTION('ref_axis',(0.,0.,-1.));
#4606=DIRECTION('center_axis',(-1.,0.,0.));
#4607=DIRECTION('ref_axis',(0.,0.,-1.));
#4608=DIRECTION('center_axis',(1.,0.,0.));
#4609=DIRECTION('ref_axis',(0.,0.,-1.));
#4610=DIRECTION('',(0.,0.,-1.));
#4611=DIRECTION('center_axis',(1.,0.,0.));
#4612=DIRECTION('ref_axis',(0.,0.,-1.));
#4613=DIRECTION('',(0.,0.,-1.));
#4614=DIRECTION('center_axis',(1.,0.,0.));
#4615=DIRECTION('ref_axis',(0.,0.,-1.));
#4616=DIRECTION('',(0.,0.,-1.));
#4617=DIRECTION('center_axis',(1.,0.,0.));
#4618=DIRECTION('ref_axis',(0.,0.,-1.));
#4619=DIRECTION('',(0.,0.,-1.));
#4620=DIRECTION('center_axis',(1.,0.,0.));
#4621=DIRECTION('ref_axis',(0.,0.,-1.));
#4622=DIRECTION('',(1.,0.,0.));
#4623=DIRECTION('center_axis',(1.,0.,0.));
#4624=DIRECTION('ref_axis',(0.,0.,-1.));
#4625=DIRECTION('center_axis',(1.,0.,0.));
#4626=DIRECTION('ref_axis',(0.,0.,-1.));
#4627=DIRECTION('',(1.,0.,0.));
#4628=DIRECTION('',(1.,0.,0.));
#4629=DIRECTION('',(1.,0.,0.));
#4630=DIRECTION('center_axis',(0.,0.,1.));
#4631=DIRECTION('ref_axis',(1.,0.,0.));
#4632=DIRECTION('center_axis',(0.,0.,-1.));
#4633=DIRECTION('ref_axis',(1.,0.,0.));
#4634=DIRECTION('',(0.,0.,1.));
#4635=DIRECTION('center_axis',(0.,0.,1.));
#4636=DIRECTION('ref_axis',(1.,0.,0.));
#4637=DIRECTION('center_axis',(1.,0.,0.));
#4638=DIRECTION('ref_axis',(0.,0.,-1.));
#4639=DIRECTION('',(1.,0.,0.));
#4640=DIRECTION('center_axis',(1.,0.,0.));
#4641=DIRECTION('ref_axis',(0.,0.,-1.));
#4642=DIRECTION('center_axis',(1.,0.,0.));
#4643=DIRECTION('ref_axis',(0.,0.,-1.));
#4644=DIRECTION('center_axis',(0.,0.,1.));
#4645=DIRECTION('ref_axis',(1.,0.,0.));
#4646=DIRECTION('center_axis',(0.,0.,1.));
#4647=DIRECTION('ref_axis',(1.,0.,0.));
#4648=DIRECTION('',(0.,0.,1.));
#4649=DIRECTION('center_axis',(0.,0.,1.));
#4650=DIRECTION('ref_axis',(1.,0.,0.));
#4651=DIRECTION('center_axis',(0.,0.,1.));
#4652=DIRECTION('ref_axis',(1.,0.,0.));
#4653=DIRECTION('center_axis',(0.,0.,1.));
#4654=DIRECTION('ref_axis',(1.,0.,0.));
#4655=DIRECTION('center_axis',(0.,0.,1.));
#4656=DIRECTION('ref_axis',(1.,0.,0.));
#4657=DIRECTION('',(0.,0.,1.));
#4658=DIRECTION('center_axis',(0.,0.,1.));
#4659=DIRECTION('ref_axis',(1.,0.,0.));
#4660=DIRECTION('center_axis',(0.,0.,1.));
#4661=DIRECTION('ref_axis',(1.,0.,0.));
#4662=DIRECTION('center_axis',(0.,0.,1.));
#4663=DIRECTION('ref_axis',(1.,0.,0.));
#4664=DIRECTION('center_axis',(0.,0.,1.));
#4665=DIRECTION('ref_axis',(1.,0.,0.));
#4666=DIRECTION('',(0.,0.,1.));
#4667=DIRECTION('center_axis',(0.,0.,1.));
#4668=DIRECTION('ref_axis',(1.,0.,0.));
#4669=DIRECTION('center_axis',(0.,0.,1.));
#4670=DIRECTION('ref_axis',(1.,0.,0.));
#4671=DIRECTION('center_axis',(0.,0.,1.));
#4672=DIRECTION('ref_axis',(1.,0.,0.));
#4673=DIRECTION('center_axis',(0.,0.,1.));
#4674=DIRECTION('ref_axis',(1.,0.,0.));
#4675=DIRECTION('',(0.,0.,1.));
#4676=DIRECTION('center_axis',(0.,0.,-1.));
#4677=DIRECTION('ref_axis',(1.,0.,0.));
#4678=DIRECTION('center_axis',(0.,0.,1.));
#4679=DIRECTION('ref_axis',(1.,0.,0.));
#4680=DIRECTION('center_axis',(0.,0.,1.));
#4681=DIRECTION('ref_axis',(-1.,1.22464679914735E-16,0.));
#4682=DIRECTION('center_axis',(0.,0.,1.));
#4683=DIRECTION('ref_axis',(1.,0.,0.));
#4684=DIRECTION('',(0.,0.,1.));
#4685=DIRECTION('',(0.,0.,1.));
#4686=DIRECTION('center_axis',(0.,0.,-1.));
#4687=DIRECTION('ref_axis',(1.,0.,0.));
#4688=DIRECTION('center_axis',(0.,0.,1.));
#4689=DIRECTION('ref_axis',(1.,0.,0.));
#4690=DIRECTION('center_axis',(0.,0.,1.));
#4691=DIRECTION('ref_axis',(1.,0.,0.));
#4692=DIRECTION('center_axis',(0.,0.,1.));
#4693=DIRECTION('ref_axis',(1.,0.,0.));
#4694=DIRECTION('',(0.,0.,-1.));
#4695=DIRECTION('',(0.,0.,-1.));
#4696=DIRECTION('center_axis',(0.,0.,1.));
#4697=DIRECTION('ref_axis',(1.,0.,0.));
#4698=DIRECTION('center_axis',(0.,0.,1.));
#4699=DIRECTION('ref_axis',(1.,0.,0.));
#4700=DIRECTION('center_axis',(0.,0.,1.));
#4701=DIRECTION('ref_axis',(1.,0.,0.));
#5726=CARTESIAN_POINT('',(0.,0.,0.));
#5727=CARTESIAN_POINT('Origin',(-6.2456986756515E-16,-3.4,3.5));
#5728=CARTESIAN_POINT('',(-0.210000000000001,-3.4,3.5));
#5729=CARTESIAN_POINT('Origin',(-6.2456986756515E-16,-3.4,3.5));
#5730=CARTESIAN_POINT('',(-0.210000000000001,-3.4,5.));
#5731=CARTESIAN_POINT('',(-0.210000000000001,-3.4,3.5));
#5732=CARTESIAN_POINT('Origin',(-6.2456986756515E-16,-3.4,5.));
#5733=CARTESIAN_POINT('Origin',(-6.38378239159465E-16,-3.4,3.5));
#5734=CARTESIAN_POINT('Origin',(2.94448637286709,1.7,3.5));
#5735=CARTESIAN_POINT('',(2.73448637286709,1.7,3.5));
#5736=CARTESIAN_POINT('Origin',(2.94448637286709,1.7,3.5));
#5737=CARTESIAN_POINT('',(2.73448637286709,1.7,5.));
#5738=CARTESIAN_POINT('',(2.73448637286709,1.7,3.5));
#5739=CARTESIAN_POINT('Origin',(2.94448637286709,1.7,5.));
#5740=CARTESIAN_POINT('Origin',(2.94448637286709,1.7,3.5));
#5741=CARTESIAN_POINT('Origin',(2.0818995585505E-16,3.4,3.5));
#5742=CARTESIAN_POINT('',(-0.21,3.4,3.5));
#5743=CARTESIAN_POINT('Origin',(2.0818995585505E-16,3.4,3.5));
#5744=CARTESIAN_POINT('',(-0.21,3.4,5.));
#5745=CARTESIAN_POINT('',(-0.21,3.4,3.5));
#5746=CARTESIAN_POINT('Origin',(2.0818995585505E-16,3.4,5.));
#5747=CARTESIAN_POINT('Origin',(2.22044604925031E-16,3.4,3.5));
#5748=CARTESIAN_POINT('Origin',(-2.94448637286709,1.7,3.5));
#5749=CARTESIAN_POINT('',(-3.15448637286709,1.7,3.5));
#5750=CARTESIAN_POINT('Origin',(-2.94448637286709,1.7,3.5));
#5751=CARTESIAN_POINT('',(-3.15448637286709,1.7,5.));
#5752=CARTESIAN_POINT('',(-3.15448637286709,1.7,3.5));
#5753=CARTESIAN_POINT('Origin',(-2.94448637286709,1.7,5.));
#5754=CARTESIAN_POINT('Origin',(-2.94448637286709,1.7,3.5));
#5755=CARTESIAN_POINT('Origin',(-2.94448637286709,-1.7,3.5));
#5756=CARTESIAN_POINT('',(-3.15448637286709,-1.7,3.5));
#5757=CARTESIAN_POINT('Origin',(-2.94448637286709,-1.7,3.5));
#5758=CARTESIAN_POINT('',(-3.15448637286709,-1.7,5.));
#5759=CARTESIAN_POINT('',(-3.15448637286709,-1.7,3.5));
#5760=CARTESIAN_POINT('Origin',(-2.94448637286709,-1.7,5.));
#5761=CARTESIAN_POINT('Origin',(-2.94448637286709,-1.7,3.5));
#5762=CARTESIAN_POINT('Origin',(2.94448637286709,-1.7,3.5));
#5763=CARTESIAN_POINT('',(2.73448637286709,-1.7,3.5));
#5764=CARTESIAN_POINT('Origin',(2.94448637286709,-1.7,3.5));
#5765=CARTESIAN_POINT('',(2.73448637286709,-1.7,5.));
#5766=CARTESIAN_POINT('',(2.73448637286709,-1.7,3.5));
#5767=CARTESIAN_POINT('Origin',(2.94448637286709,-1.7,5.));
#5768=CARTESIAN_POINT('Origin',(2.94448637286709,-1.7,3.5));
#5769=CARTESIAN_POINT('Origin',(-0.1,0.,3.9));
#5770=CARTESIAN_POINT('',(2.5,0.,3.5));
#5771=CARTESIAN_POINT('',(2.5,0.,4.3));
#5772=CARTESIAN_POINT('Origin',(2.5,0.,3.9));
#5773=CARTESIAN_POINT('Ctrl Pts',(2.5,2.77555756156289E-17,4.3));
#5774=CARTESIAN_POINT('Ctrl Pts',(2.5,-0.0503173531062473,4.3));
#5775=CARTESIAN_POINT('Ctrl Pts',(2.49832635585429,-0.103929980260481,4.28992638341895));
#5776=CARTESIAN_POINT('Ctrl Pts',(2.49227754123301,-0.202456609487086,4.24907785041389));
#5777=CARTESIAN_POINT('Ctrl Pts',(2.48798680132732,-0.247377744540872,4.21830768040837));
#5778=CARTESIAN_POINT('Ctrl Pts',(2.47991004659989,-0.318308483288254,4.14737694166098));
#5779=CARTESIAN_POINT('Ctrl Pts',(2.47559507764305,-0.3490780234852,4.10245615200085));
#5780=CARTESIAN_POINT('Ctrl Pts',(2.46949065540042,-0.389926098864548,4.00393070664371));
#5781=CARTESIAN_POINT('Ctrl Pts',(2.46779253585061,-0.4,3.95031849222446));
#5782=CARTESIAN_POINT('Ctrl Pts',(2.46779253585061,-0.4,3.84968150777554));
#5783=CARTESIAN_POINT('Ctrl Pts',(2.46949065540042,-0.389926098864548,3.79606929335629));
#5784=CARTESIAN_POINT('Ctrl Pts',(2.47559507764305,-0.3490780234852,3.69754384799915));
#5785=CARTESIAN_POINT('Ctrl Pts',(2.47991004659989,-0.318308483288254,3.65262305833902));
#5786=CARTESIAN_POINT('Ctrl Pts',(2.48798680132732,-0.247377744540872,3.58169231959163));
#5787=CARTESIAN_POINT('Ctrl Pts',(2.49227754123301,-0.202456609487086,3.55092214958611));
#5788=CARTESIAN_POINT('Ctrl Pts',(2.49832635585429,-0.103929980260481,3.51007361658105));
#5789=CARTESIAN_POINT('Ctrl Pts',(2.5,-0.0503173531062475,3.5));
#5790=CARTESIAN_POINT('Ctrl Pts',(2.5,-1.52655665885959E-16,3.5));
#5791=CARTESIAN_POINT('Origin',(-0.1,0.,3.9));
#5792=CARTESIAN_POINT('Origin',(2.5,0.,3.9));
#5793=CARTESIAN_POINT('Ctrl Pts',(2.5,-2.77555756156289E-17,3.5));
#5794=CARTESIAN_POINT('Ctrl Pts',(2.5,0.0503173531062474,3.5));
#5795=CARTESIAN_POINT('Ctrl Pts',(2.49832635585429,0.103929980260481,3.51007361658105));
#5796=CARTESIAN_POINT('Ctrl Pts',(2.49227754123301,0.202456609487086,3.55092214958611));
#5797=CARTESIAN_POINT('Ctrl Pts',(2.48798680132732,0.247377744540872,3.58169231959163));
#5798=CARTESIAN_POINT('Ctrl Pts',(2.47991004659989,0.318308483288254,3.65262305833902));
#5799=CARTESIAN_POINT('Ctrl Pts',(2.47559507764305,0.3490780234852,3.69754384799915));
#5800=CARTESIAN_POINT('Ctrl Pts',(2.46949065540042,0.389926098864548,3.79606929335629));
#5801=CARTESIAN_POINT('Ctrl Pts',(2.46779253585061,0.4,3.84968150777554));
#5802=CARTESIAN_POINT('Ctrl Pts',(2.46779253585061,0.4,3.9));
#5803=CARTESIAN_POINT('Ctrl Pts',(2.46779253585061,0.4,3.95031849222446));
#5804=CARTESIAN_POINT('Ctrl Pts',(2.46949065540042,0.389926098864548,4.00393070664371));
#5805=CARTESIAN_POINT('Ctrl Pts',(2.47559507764305,0.3490780234852,4.10245615200085));
#5806=CARTESIAN_POINT('Ctrl Pts',(2.47991004659989,0.318308483288254,4.14737694166098));
#5807=CARTESIAN_POINT('Ctrl Pts',(2.48798680132732,0.247377744540872,4.21830768040837));
#5808=CARTESIAN_POINT('Ctrl Pts',(2.49227754123301,0.202456609487086,4.24907785041389));
#5809=CARTESIAN_POINT('Ctrl Pts',(2.49832635585429,0.103929980260481,4.28992638341895));
#5810=CARTESIAN_POINT('Ctrl Pts',(2.5,0.0503173531062475,4.3));
#5811=CARTESIAN_POINT('Ctrl Pts',(2.5,8.32667268468867E-17,4.3));
#5812=CARTESIAN_POINT('Origin',(2.5,0.,3.9));
#5813=CARTESIAN_POINT('',(2.5,-8.38883057415937E-17,4.585));
#5814=CARTESIAN_POINT('',(2.5,0.,3.2));
#5815=CARTESIAN_POINT('',(2.5,0.,3.215));
#5816=CARTESIAN_POINT('Origin',(2.5,0.,3.9));
#5817=CARTESIAN_POINT('',(2.5,0.,3.2));
#5818=CARTESIAN_POINT('Origin',(2.5,0.,3.9));
#5819=CARTESIAN_POINT('',(2.5,0.,3.2));
#5820=CARTESIAN_POINT('Origin',(2.5,0.,3.9));
#5821=CARTESIAN_POINT('',(2.5,0.,3.2));
#5822=CARTESIAN_POINT('Origin',(2.5,0.,3.9));
#5823=CARTESIAN_POINT('',(4.,-8.38883057415937E-17,4.585));
#5824=CARTESIAN_POINT('',(2.5,-8.38883057415937E-17,4.585));
#5825=CARTESIAN_POINT('',(3.94091042780726,0.685,3.9));
#5826=CARTESIAN_POINT('Ctrl Pts',(3.94091042780726,0.685,3.9));
#5827=CARTESIAN_POINT('Ctrl Pts',(3.94091042780726,0.685,3.81380574680012));
#5828=CARTESIAN_POINT('Ctrl Pts',(3.94403084813346,0.667739203937252,3.7219849815769));
#5829=CARTESIAN_POINT('Ctrl Pts',(3.95523876756334,0.597780269847898,3.55326702036063));
#5830=CARTESIAN_POINT('Ctrl Pts',(3.96315754832666,0.545091192335771,3.4763549021102));
#5831=CARTESIAN_POINT('Ctrl Pts',(3.97797250301845,0.423646908301837,3.35491061807627));
#5832=CARTESIAN_POINT('Ctrl Pts',(3.98584030517825,0.346734013912698,3.30222012067742));
#5833=CARTESIAN_POINT('Ctrl Pts',(3.99693115404432,0.178013382290042,3.2322601559763));
#5834=CARTESIAN_POINT('Ctrl Pts',(4.,0.086191683382974,3.215));
#5835=CARTESIAN_POINT('Ctrl Pts',(4.,-0.086191683382974,3.215));
#5836=CARTESIAN_POINT('Ctrl Pts',(3.99693115404432,-0.178013382290042,3.2322601559763));
#5837=CARTESIAN_POINT('Ctrl Pts',(3.98584030517825,-0.346734013912697,3.30222012067742));
#5838=CARTESIAN_POINT('Ctrl Pts',(3.97797250301845,-0.423646908301837,3.35491061807627));
#5839=CARTESIAN_POINT('Ctrl Pts',(3.96315754832666,-0.545091192335771,3.4763549021102));
#5840=CARTESIAN_POINT('Ctrl Pts',(3.95523876756334,-0.597780269847898,3.55326702036063));
#5841=CARTESIAN_POINT('Ctrl Pts',(3.94403084813346,-0.667739203937252,3.7219849815769));
#5842=CARTESIAN_POINT('Ctrl Pts',(3.94091042780726,-0.685,3.81380574680012));
#5843=CARTESIAN_POINT('Ctrl Pts',(3.94091042780726,-0.685,3.98619425319988));
#5844=CARTESIAN_POINT('Ctrl Pts',(3.94403084813346,-0.667739203937252,4.0780150184231));
#5845=CARTESIAN_POINT('Ctrl Pts',(3.95523876756334,-0.597780269847898,4.24673297963937));
#5846=CARTESIAN_POINT('Ctrl Pts',(3.96315754832666,-0.545091192335771,4.3236450978898));
#5847=CARTESIAN_POINT('Ctrl Pts',(3.97797250301844,-0.423646908301837,4.44508938192373));
#5848=CARTESIAN_POINT('Ctrl Pts',(3.98584030517825,-0.346734013912698,4.49777987932258));
#5849=CARTESIAN_POINT('Ctrl Pts',(3.99693115404432,-0.178013382290042,4.5677398440237));
#5850=CARTESIAN_POINT('Ctrl Pts',(4.,-0.0861916833829741,4.585));
#5851=CARTESIAN_POINT('Ctrl Pts',(4.,0.,4.585));
#5852=CARTESIAN_POINT('Ctrl Pts',(4.,-1.94289029309402E-16,4.585));
#5853=CARTESIAN_POINT('Ctrl Pts',(4.,0.0861916833829739,4.585));
#5854=CARTESIAN_POINT('Ctrl Pts',(3.99693115404432,0.178013382290042,4.5677398440237));
#5855=CARTESIAN_POINT('Ctrl Pts',(3.98584030517825,0.346734013912697,4.49777987932258));
#5856=CARTESIAN_POINT('Ctrl Pts',(3.97797250301844,0.423646908301837,4.44508938192373));
#5857=CARTESIAN_POINT('Ctrl Pts',(3.96315754832666,0.545091192335771,4.3236450978898));
#5858=CARTESIAN_POINT('Ctrl Pts',(3.95523876756334,0.597780269847898,4.24673297963937));
#5859=CARTESIAN_POINT('Ctrl Pts',(3.94403084813346,0.667739203937252,4.0780150184231));
#5860=CARTESIAN_POINT('Ctrl Pts',(3.94091042780726,0.685,3.98619425319988));
#5861=CARTESIAN_POINT('Ctrl Pts',(3.94091042780726,0.685,3.9));
#5862=CARTESIAN_POINT('Origin',(-2.6,0.,1.9));
#5863=CARTESIAN_POINT('',(-2.5,-4.89858719658941E-17,2.3));
#5864=CARTESIAN_POINT('Origin',(-2.5,0.,1.9));
#5865=CARTESIAN_POINT('',(-0.8,-5.91874055024832E-17,2.3));
#5866=CARTESIAN_POINT('',(-2.6,-4.89858719658941E-17,2.3));
#5867=CARTESIAN_POINT('',(-0.8,9.79717439317883E-17,1.5));
#5868=CARTESIAN_POINT('Ctrl Pts',(-0.8,-1.38777878078145E-17,1.5));
#5869=CARTESIAN_POINT('Ctrl Pts',(-0.8,-0.0511821204434756,1.5));
#5870=CARTESIAN_POINT('Ctrl Pts',(-0.794636787340262,-0.105178030195542,
1.51041443765235));
#5871=CARTESIAN_POINT('Ctrl Pts',(-0.775305936415791,-0.20349630324575,
1.55153396803017));
#5872=CARTESIAN_POINT('Ctrl Pts',(-0.761546644028199,-0.247878667922505,
1.58219324297327));
#5873=CARTESIAN_POINT('Ctrl Pts',(-0.735080187019535,-0.317902331252414,
1.65221690630318));
#5874=CARTESIAN_POINT('Ctrl Pts',(-0.720478404984272,-0.34849148389449,
1.69656705619687));
#5875=CARTESIAN_POINT('Ctrl Pts',(-0.699130174381174,-0.389554233790704,
1.79474455949469));
#5876=CARTESIAN_POINT('Ctrl Pts',(-0.692820323027551,-0.4,1.8486779732158));
#5877=CARTESIAN_POINT('Ctrl Pts',(-0.692820323027551,-0.4,1.9513220267842));
#5878=CARTESIAN_POINT('Ctrl Pts',(-0.699130174381174,-0.389554233790704,
2.00525544050531));
#5879=CARTESIAN_POINT('Ctrl Pts',(-0.720478404984272,-0.348491483894491,
2.10343294380313));
#5880=CARTESIAN_POINT('Ctrl Pts',(-0.735080187019535,-0.317902331252414,
2.14778309369682));
#5881=CARTESIAN_POINT('Ctrl Pts',(-0.761546644028199,-0.247878667922505,
2.21780675702673));
#5882=CARTESIAN_POINT('Ctrl Pts',(-0.775305936415791,-0.20349630324575,
2.24846603196983));
#5883=CARTESIAN_POINT('Ctrl Pts',(-0.794636787340262,-0.105178030195542,
2.28958556234765));
#5884=CARTESIAN_POINT('Ctrl Pts',(-0.8,-0.0511821204434756,2.3));
#5885=CARTESIAN_POINT('Ctrl Pts',(-0.8,-6.93889390390723E-17,2.3));
#5886=CARTESIAN_POINT('',(-0.925,-1.1327982892113E-16,1.5));
#5887=CARTESIAN_POINT('',(-2.6,0.,1.5));
#5888=CARTESIAN_POINT('',(-2.6,0.,1.5));
#5889=CARTESIAN_POINT('Ctrl Pts',(-0.8,-8.32667268468867E-17,2.3));
#5890=CARTESIAN_POINT('Ctrl Pts',(-0.8,0.0511821204434754,2.3));
#5891=CARTESIAN_POINT('Ctrl Pts',(-0.794636787340262,0.105178030195542,
2.28958556234765));
#5892=CARTESIAN_POINT('Ctrl Pts',(-0.775305936415791,0.20349630324575,2.24846603196983));
#5893=CARTESIAN_POINT('Ctrl Pts',(-0.761546644028199,0.247878667922505,
2.21780675702673));
#5894=CARTESIAN_POINT('Ctrl Pts',(-0.735080187019535,0.317902331252414,
2.14778309369682));
#5895=CARTESIAN_POINT('Ctrl Pts',(-0.720478404984272,0.348491483894491,
2.10343294380313));
#5896=CARTESIAN_POINT('Ctrl Pts',(-0.699130174381174,0.389554233790704,
2.00525544050531));
#5897=CARTESIAN_POINT('Ctrl Pts',(-0.692820323027551,0.4,1.9513220267842));
#5898=CARTESIAN_POINT('Ctrl Pts',(-0.692820323027551,0.4,1.9));
#5899=CARTESIAN_POINT('Ctrl Pts',(-0.692820323027551,0.4,1.8486779732158));
#5900=CARTESIAN_POINT('Ctrl Pts',(-0.699130174381174,0.389554233790704,
1.79474455949469));
#5901=CARTESIAN_POINT('Ctrl Pts',(-0.720478404984272,0.34849148389449,1.69656705619687));
#5902=CARTESIAN_POINT('Ctrl Pts',(-0.735080187019535,0.317902331252414,
1.65221690630318));
#5903=CARTESIAN_POINT('Ctrl Pts',(-0.761546644028199,0.247878667922505,
1.58219324297327));
#5904=CARTESIAN_POINT('Ctrl Pts',(-0.775305936415792,0.20349630324575,1.55153396803017));
#5905=CARTESIAN_POINT('Ctrl Pts',(-0.794636787340262,0.105178030195542,
1.51041443765235));
#5906=CARTESIAN_POINT('Ctrl Pts',(-0.8,0.0511821204434755,1.5));
#5907=CARTESIAN_POINT('Ctrl Pts',(-0.8,-5.55111512312578E-17,1.5));
#5908=CARTESIAN_POINT('Origin',(0.,0.,1.4));
#5909=CARTESIAN_POINT('Origin',(0.,0.,1.5));
#5910=CARTESIAN_POINT('',(-0.8,-9.79717439317883E-17,2.4));
#5911=CARTESIAN_POINT('',(-0.8,-9.79717439317883E-17,1.4));
#5912=CARTESIAN_POINT('Origin',(0.,0.,2.4));
#5913=CARTESIAN_POINT('Origin',(-4.1,0.,1.9));
#5914=CARTESIAN_POINT('',(-3.94091042780726,0.685,1.9));
#5915=CARTESIAN_POINT('',(-4.,-8.38883057415937E-17,2.585));
#5916=CARTESIAN_POINT('Ctrl Pts',(-3.94091042780726,0.685,1.9));
#5917=CARTESIAN_POINT('Ctrl Pts',(-3.94091042780726,0.685,1.98619425319988));
#5918=CARTESIAN_POINT('Ctrl Pts',(-3.94403084813346,0.667739203937252,2.07801501842309));
#5919=CARTESIAN_POINT('Ctrl Pts',(-3.95523876756334,0.597780269847899,2.24673297963937));
#5920=CARTESIAN_POINT('Ctrl Pts',(-3.96315754832666,0.545091192335771,2.3236450978898));
#5921=CARTESIAN_POINT('Ctrl Pts',(-3.97797250301844,0.423646908301837,2.44508938192373));
#5922=CARTESIAN_POINT('Ctrl Pts',(-3.98584030517825,0.346734013912698,2.49777987932258));
#5923=CARTESIAN_POINT('Ctrl Pts',(-3.99693115404432,0.178013382290042,2.5677398440237));
#5924=CARTESIAN_POINT('Ctrl Pts',(-4.,0.0861916833829741,2.585));
#5925=CARTESIAN_POINT('Ctrl Pts',(-4.,2.77555756156289E-17,2.585));
#5926=CARTESIAN_POINT('',(-4.,-3.14318298868543E-16,1.215));
#5927=CARTESIAN_POINT('Ctrl Pts',(-4.,-1.38777878078145E-16,1.215));
#5928=CARTESIAN_POINT('Ctrl Pts',(-4.,0.0861916833829738,1.215));
#5929=CARTESIAN_POINT('Ctrl Pts',(-3.99693115404432,0.178013382290042,1.2322601559763));
#5930=CARTESIAN_POINT('Ctrl Pts',(-3.98584030517825,0.346734013912697,1.30222012067742));
#5931=CARTESIAN_POINT('Ctrl Pts',(-3.97797250301844,0.423646908301837,1.35491061807627));
#5932=CARTESIAN_POINT('Ctrl Pts',(-3.96315754832666,0.545091192335771,1.4763549021102));
#5933=CARTESIAN_POINT('Ctrl Pts',(-3.95523876756334,0.597780269847898,1.55326702036063));
#5934=CARTESIAN_POINT('Ctrl Pts',(-3.94403084813346,0.667739203937252,1.7219849815769));
#5935=CARTESIAN_POINT('Ctrl Pts',(-3.94091042780726,0.685,1.81380574680012));
#5936=CARTESIAN_POINT('Ctrl Pts',(-3.94091042780726,0.685,1.9));
#5937=CARTESIAN_POINT('Ctrl Pts',(-4.,1.11022302462516E-16,2.585));
#5938=CARTESIAN_POINT('Ctrl Pts',(-4.,-0.0861916833829739,2.585));
#5939=CARTESIAN_POINT('Ctrl Pts',(-3.99693115404432,-0.178013382290042,
2.5677398440237));
#5940=CARTESIAN_POINT('Ctrl Pts',(-3.98584030517825,-0.346734013912697,
2.49777987932258));
#5941=CARTESIAN_POINT('Ctrl Pts',(-3.97797250301844,-0.423646908301837,
2.44508938192373));
#5942=CARTESIAN_POINT('Ctrl Pts',(-3.96315754832666,-0.545091192335771,
2.3236450978898));
#5943=CARTESIAN_POINT('Ctrl Pts',(-3.95523876756334,-0.597780269847899,
2.24673297963937));
#5944=CARTESIAN_POINT('Ctrl Pts',(-3.94403084813346,-0.667739203937252,
2.07801501842309));
#5945=CARTESIAN_POINT('Ctrl Pts',(-3.94091042780726,-0.685,1.98619425319988));
#5946=CARTESIAN_POINT('Ctrl Pts',(-3.94091042780726,-0.685,1.81380574680012));
#5947=CARTESIAN_POINT('Ctrl Pts',(-3.94403084813346,-0.667739203937252,
1.7219849815769));
#5948=CARTESIAN_POINT('Ctrl Pts',(-3.95523876756334,-0.597780269847898,
1.55326702036063));
#5949=CARTESIAN_POINT('Ctrl Pts',(-3.96315754832666,-0.545091192335771,
1.4763549021102));
#5950=CARTESIAN_POINT('Ctrl Pts',(-3.97797250301844,-0.423646908301837,
1.35491061807627));
#5951=CARTESIAN_POINT('Ctrl Pts',(-3.98584030517825,-0.346734013912697,
1.30222012067742));
#5952=CARTESIAN_POINT('Ctrl Pts',(-3.99693115404432,-0.178013382290042,
1.2322601559763));
#5953=CARTESIAN_POINT('Ctrl Pts',(-4.,-0.0861916833829742,1.215));
#5954=CARTESIAN_POINT('Ctrl Pts',(-4.,-2.22044604925031E-16,1.215));
#5955=CARTESIAN_POINT('',(-2.5,-8.38883057415937E-17,2.585));
#5956=CARTESIAN_POINT('',(-4.1,-8.38883057415937E-17,2.585));
#5957=CARTESIAN_POINT('Origin',(-2.5,0.,1.9));
#5958=CARTESIAN_POINT('Origin',(-2.5,0.,1.9));
#5959=CARTESIAN_POINT('Origin',(0.,-3.,0.9));
#5960=CARTESIAN_POINT('',(-0.165,-3.,1.));
#5961=CARTESIAN_POINT('Origin',(0.,-3.,1.));
#5962=CARTESIAN_POINT('',(-0.165,-3.,2.1));
#5963=CARTESIAN_POINT('',(-0.165,-3.,0.9));
#5964=CARTESIAN_POINT('Origin',(0.,-3.,2.1));
#5965=CARTESIAN_POINT('Origin',(0.,-3.,2.1));
#5966=CARTESIAN_POINT('Origin',(0.,3.,0.9));
#5967=CARTESIAN_POINT('',(-0.165,3.,1.));
#5968=CARTESIAN_POINT('Origin',(0.,3.,1.));
#5969=CARTESIAN_POINT('',(-0.165,3.,2.1));
#5970=CARTESIAN_POINT('',(-0.165,3.,0.9));
#5971=CARTESIAN_POINT('Origin',(0.,3.,2.1));
#5972=CARTESIAN_POINT('Origin',(0.,3.,2.1));
#5973=CARTESIAN_POINT('Origin',(0.,0.,0.9));
#5974=CARTESIAN_POINT('',(-0.925,-1.1327982892113E-16,1.));
#5975=CARTESIAN_POINT('Origin',(0.,0.,1.));
#5976=CARTESIAN_POINT('',(-0.925,-1.1327982892113E-16,0.9));
#5977=CARTESIAN_POINT('Origin',(0.,0.,1.5));
#5978=CARTESIAN_POINT('Origin',(0.,0.,1.5));
#5979=CARTESIAN_POINT('Origin',(0.,0.,2.3));
#5980=CARTESIAN_POINT('',(-0.6,-7.34788079488412E-17,2.4));
#5981=CARTESIAN_POINT('Origin',(0.,0.,2.4));
#5982=CARTESIAN_POINT('',(-0.6,7.34788079488412E-17,3.2));
#5983=CARTESIAN_POINT('',(-0.6,-7.34788079488412E-17,2.3));
#5984=CARTESIAN_POINT('Origin',(0.,0.,3.2));
#5985=CARTESIAN_POINT('Origin',(0.,0.,2.4));
#5986=CARTESIAN_POINT('Origin',(0.,0.,3.2));
#5987=CARTESIAN_POINT('',(2.5,0.,3.2));
#5988=CARTESIAN_POINT('Origin',(0.,0.,3.2));
#5989=CARTESIAN_POINT('',(2.5,0.,3.2));
#5990=CARTESIAN_POINT('',(2.5,0.,5.));
#5991=CARTESIAN_POINT('',(2.5,0.,3.2));
#5992=CARTESIAN_POINT('Origin',(0.,0.,5.));
#5993=CARTESIAN_POINT('Origin',(0.,0.,3.2));
#5994=CARTESIAN_POINT('Origin',(0.,0.,1.));
#5995=CARTESIAN_POINT('',(-4.,-4.89858719658941E-16,5.));
#5996=CARTESIAN_POINT('Origin',(0.,0.,5.));
#5997=CARTESIAN_POINT('',(-4.,-4.89858719658941E-16,1.));
#5998=CARTESIAN_POINT('',(-4.,-4.89858719658941E-16,1.));
#5999=CARTESIAN_POINT('',(-4.,-4.89858719658941E-16,1.));
#6000=CARTESIAN_POINT('Origin',(0.,0.,1.));
#6001=CARTESIAN_POINT('Origin',(0.,0.,5.));
#6002=CARTESIAN_POINT('Origin',(0.,0.,1.));
#8381=UNCERTAINTY_MEASURE_WITH_UNIT(LENGTH_MEASURE(0.001),#8429,
'DISTANCE_ACCURACY_VALUE',
'Maximum model space distance between geometric entities at asserted c
onnectivities');
#8402=UNCERTAINTY_MEASURE_WITH_UNIT(LENGTH_MEASURE(0.001),#8429,
'DISTANCE_ACCURACY_VALUE',
'Maximum model space distance between geometric entities at asserted c
onnectivities');
#8407=(
GEOMETRIC_REPRESENTATION_CONTEXT(3)
GLOBAL_UNCERTAINTY_ASSIGNED_CONTEXT((#8381))
GLOBAL_UNIT_ASSIGNED_CONTEXT((#8429,#8431,#8432))
REPRESENTATION_CONTEXT('','3D')
);
#8428=(
GEOMETRIC_REPRESENTATION_CONTEXT(3)
GLOBAL_UNCERTAINTY_ASSIGNED_CONTEXT((#8402))
GLOBAL_UNIT_ASSIGNED_CONTEXT((#8429,#8431,#8432))
REPRESENTATION_CONTEXT('','3D')
);
#8429=(
LENGTH_UNIT()
NAMED_UNIT(*)
SI_UNIT(.CENTI.,.METRE.)
);
#8431=(
NAMED_UNIT(*)
PLANE_ANGLE_UNIT()
SI_UNIT($,.RADIAN.)
);
#8432=(
NAMED_UNIT(*)
SI_UNIT($,.STERADIAN.)
SOLID_ANGLE_UNIT()
);
#8437=SHAPE_DEFINITION_REPRESENTATION(#8462,#8518);
#8462=PRODUCT_DEFINITION_SHAPE('',$,#8544);
#8518=SHAPE_REPRESENTATION('',(#4000),#8407);
#8539=PRODUCT_DEFINITION_CONTEXT('part definition',#8616,'design');
#8544=PRODUCT_DEFINITION('Lower body','Lower body',#8569,
#8539);
#8569=PRODUCT_DEFINITION_FORMATION('',$,#8622);
#8616=APPLICATION_CONTEXT(
'Core Data for Automotive Mechanical Design Process');
#8617=PRODUCT_CONTEXT('part definition',#8616,'mechanical');
#8622=PRODUCT('Lower body','Lower body','Lower body',(#8617));
#8678=COLOUR_RGB('Dark Blue',0.08,0.2,0.34);
#8679=FILL_AREA_STYLE_COLOUR('',#8678);
#8680=FILL_AREA_STYLE('',(#8679));
#8681=SURFACE_STYLE_FILL_AREA(#8680);
#8682=SURFACE_SIDE_STYLE('',(#8681));
#8683=SURFACE_STYLE_USAGE(.BOTH.,#8682);
#8684=PRESENTATION_STYLE_ASSIGNMENT((#8683));
ENDSEC;
END-ISO-10303-21;
